ISO-10303-21;
HEADER;
/* Generated by software containing ST-Developer
 * from STEP Tools, Inc. (www.steptools.com) 
 */

FILE_DESCRIPTION(
/* description */ ('Worm-less right-angle friction wheel drive'),
/* implementation_level */ '2;1');

FILE_NAME(
/* name */ 'Foot strip (1).step',
/* time_stamp */ '2026-10-28T03:22:36-07:00',
/* author */ (''),
/* organization */ (''),
/* preprocessor_version */ 'ST-DEVELOPER v20.2',
/* originating_system */ 'Autodesk Translation Framework v15.17.0.0',
/* authorisation */ '');

FILE_SCHEMA (('AUTOMOTIVE_DESIGN { 1 0 10303 214 3 1 1 }'));
ENDSEC;

DATA;
#10=MECHANICAL_DESIGN_GEOMETRIC_PRESENTATION_REPRESENTATION('',(#613),#17046);
#519=SHAPE_REPRESENTATION_RELATIONSHIP('SRR','None',#17262,#566);
#566=ADVANCED_BREP_SHAPE_REPRESENTATION('',(#667),#16998);
#613=STYLED_ITEM('',(#17577),#667);
#667=MANIFOLD_SOLID_BREP('Body1',#8168);
#964=PLANE('',#8789);
#965=PLANE('',#8790);
#966=PLANE('',#8791);
#967=PLANE('',#8792);
#968=PLANE('',#8793);
#969=PLANE('',#8794);
#1230=FACE_OUTER_BOUND('',#1716,.T.);
#1231=FACE_OUTER_BOUND('',#1717,.T.);
#1232=FACE_OUTER_BOUND('',#1718,.T.);
#1233=FACE_OUTER_BOUND('',#1719,.T.);
#1234=FACE_OUTER_BOUND('',#1720,.T.);
#1235=FACE_OUTER_BOUND('',#1721,.T.);
#1716=EDGE_LOOP('',(#5642,#5643,#5644,#5645));
#1717=EDGE_LOOP('',(#5646,#5647,#5648,#5649));
#1718=EDGE_LOOP('',(#5650,#5651,#5652,#5653));
#1719=EDGE_LOOP('',(#5654,#5655,#5656,#5657));
#1720=EDGE_LOOP('',(#5658,#5659,#5660,#5661));
#1721=EDGE_LOOP('',(#5662,#5663,#5664,#5665));
#2411=LINE('',#12495,#2951);
#2412=LINE('',#12497,#2952);
#2413=LINE('',#12499,#2953);
#2414=LINE('',#12500,#2954);
#2415=LINE('',#12503,#2955);
#2416=LINE('',#12505,#2956);
#2417=LINE('',#12506,#2957);
#2418=LINE('',#12509,#2958);
#2419=LINE('',#12511,#2959);
#2420=LINE('',#12512,#2960);
#2421=LINE('',#12514,#2961);
#2422=LINE('',#12515,#2962);
#2951=VECTOR('',#9903,1.);
#2952=VECTOR('',#9904,1.);
#2953=VECTOR('',#9905,1.);
#2954=VECTOR('',#9906,1.);
#2955=VECTOR('',#9909,1.);
#2956=VECTOR('',#9910,1.);
#2957=VECTOR('',#9911,1.);
#2958=VECTOR('',#9914,1.);
#2959=VECTOR('',#9915,1.);
#2960=VECTOR('',#9916,1.);
#2961=VECTOR('',#9919,1.);
#2962=VECTOR('',#9920,1.);
#3905=VERTEX_POINT('',#12493);
#3906=VERTEX_POINT('',#12494);
#3907=VERTEX_POINT('',#12496);
#3908=VERTEX_POINT('',#12498);
#3909=VERTEX_POINT('',#12502);
#3910=VERTEX_POINT('',#12504);
#3911=VERTEX_POINT('',#12508);
#3912=VERTEX_POINT('',#12510);
#4590=EDGE_CURVE('',#3905,#3906,#2411,.T.);
#4591=EDGE_CURVE('',#3906,#3907,#2412,.T.);
#4592=EDGE_CURVE('',#3908,#3907,#2413,.T.);
#4593=EDGE_CURVE('',#3905,#3908,#2414,.T.);
#4594=EDGE_CURVE('',#3909,#3905,#2415,.T.);
#4595=EDGE_CURVE('',#3910,#3908,#2416,.T.);
#4596=EDGE_CURVE('',#3909,#3910,#2417,.T.);
#4597=EDGE_CURVE('',#3911,#3909,#2418,.T.);
#4598=EDGE_CURVE('',#3912,#3910,#2419,.T.);
#4599=EDGE_CURVE('',#3911,#3912,#2420,.T.);
#4600=EDGE_CURVE('',#3906,#3911,#2421,.T.);
#4601=EDGE_CURVE('',#3907,#3912,#2422,.T.);
#5642=ORIENTED_EDGE('',*,*,#4590,.T.);
#5643=ORIENTED_EDGE('',*,*,#4591,.T.);
#5644=ORIENTED_EDGE('',*,*,#4592,.F.);
#5645=ORIENTED_EDGE('',*,*,#4593,.F.);
#5646=ORIENTED_EDGE('',*,*,#4594,.T.);
#5647=ORIENTED_EDGE('',*,*,#4593,.T.);
#5648=ORIENTED_EDGE('',*,*,#4595,.F.);
#5649=ORIENTED_EDGE('',*,*,#4596,.F.);
#5650=ORIENTED_EDGE('',*,*,#4597,.T.);
#5651=ORIENTED_EDGE('',*,*,#4596,.T.);
#5652=ORIENTED_EDGE('',*,*,#4598,.F.);
#5653=ORIENTED_EDGE('',*,*,#4599,.F.);
#5654=ORIENTED_EDGE('',*,*,#4600,.T.);
#5655=ORIENTED_EDGE('',*,*,#4599,.T.);
#5656=ORIENTED_EDGE('',*,*,#4601,.F.);
#5657=ORIENTED_EDGE('',*,*,#4591,.F.);
#5658=ORIENTED_EDGE('',*,*,#4601,.T.);
#5659=ORIENTED_EDGE('',*,*,#4598,.T.);
#5660=ORIENTED_EDGE('',*,*,#4595,.T.);
#5661=ORIENTED_EDGE('',*,*,#4592,.T.);
#5662=ORIENTED_EDGE('',*,*,#4600,.F.);
#5663=ORIENTED_EDGE('',*,*,#4590,.F.);
#5664=ORIENTED_EDGE('',*,*,#4594,.F.);
#5665=ORIENTED_EDGE('',*,*,#4597,.F.);
#7722=ADVANCED_FACE('',(#1230),#964,.T.);
#7723=ADVANCED_FACE('',(#1231),#965,.T.);
#7724=ADVANCED_FACE('',(#1232),#966,.T.);
#7725=ADVANCED_FACE('',(#1233),#967,.T.);
#7726=ADVANCED_FACE('',(#1234),#968,.T.);
#7727=ADVANCED_FACE('',(#1235),#969,.F.);
#8168=CLOSED_SHELL('',(#7722,#7723,#7724,#7725,#7726,#7727));
#8788=AXIS2_PLACEMENT_3D('',#12491,#9899,#9900);
#8789=AXIS2_PLACEMENT_3D('',#12492,#9901,#9902);
#8790=AXIS2_PLACEMENT_3D('',#12501,#9907,#9908);
#8791=AXIS2_PLACEMENT_3D('',#12507,#9912,#9913);
#8792=AXIS2_PLACEMENT_3D('',#12513,#9917,#9918);
#8793=AXIS2_PLACEMENT_3D('',#12516,#9921,#9922);
#8794=AXIS2_PLACEMENT_3D('',#12517,#9923,#9924);
#9899=DIRECTION('axis',(0.,0.,1.));
#9900=DIRECTION('refdir',(1.,0.,0.));
#9901=DIRECTION('center_axis',(0.,1.,0.));
#9902=DIRECTION('ref_axis',(-1.,0.,0.));
#9903=DIRECTION('',(-1.,0.,0.));
#9904=DIRECTION('',(0.,0.,1.));
#9905=DIRECTION('',(-1.,0.,0.));
#9906=DIRECTION('',(0.,0.,1.));
#9907=DIRECTION('center_axis',(1.,0.,0.));
#9908=DIRECTION('ref_axis',(0.,1.,0.));
#9909=DIRECTION('',(0.,1.,0.));
#9910=DIRECTION('',(0.,1.,0.));
#9911=DIRECTION('',(0.,0.,1.));
#9912=DIRECTION('center_axis',(0.,-1.,0.));
#9913=DIRECTION('ref_axis',(1.,0.,0.));
#9914=DIRECTION('',(1.,0.,0.));
#9915=DIRECTION('',(1.,0.,0.));
#9916=DIRECTION('',(0.,0.,1.));
#9917=DIRECTION('center_axis',(-1.,0.,0.));
#9918=DIRECTION('ref_axis',(0.,-1.,0.));
#9919=DIRECTION('',(0.,-1.,0.));
#9920=DIRECTION('',(0.,-1.,0.));
#9921=DIRECTION('center_axis',(0.,0.,1.));
#9922=DIRECTION('ref_axis',(1.,0.,0.));
#9923=DIRECTION('center_axis',(0.,0.,1.));
#9924=DIRECTION('ref_axis',(1.,0.,0.));
#12491=CARTESIAN_POINT('',(0.,0.,0.));
#12492=CARTESIAN_POINT('Origin',(10.,10.5,-0.4));
#12493=CARTESIAN_POINT('',(10.,10.5,-0.4));
#12494=CARTESIAN_POINT('',(-6.,10.5,-0.4));
#12495=CARTESIAN_POINT('',(10.,10.5,-0.4));
#12496=CARTESIAN_POINT('',(-6.,10.5,0.));
#12497=CARTESIAN_POINT('',(-6.,10.5,-0.4));
#12498=CARTESIAN_POINT('',(10.,10.5,0.));
#12499=CARTESIAN_POINT('',(10.,10.5,0.));
#12500=CARTESIAN_POINT('',(10.,10.5,-0.4));
#12501=CARTESIAN_POINT('Origin',(10.,9.5,-0.4));
#12502=CARTESIAN_POINT('',(10.,9.5,-0.4));
#12503=CARTESIAN_POINT('',(10.,9.5,-0.4));
#12504=CARTESIAN_POINT('',(10.,9.5,0.));
#12505=CARTESIAN_POINT('',(10.,9.5,0.));
#12506=CARTESIAN_POINT('',(10.,9.5,-0.4));
#12507=CARTESIAN_POINT('Origin',(-6.,9.5,-0.4));
#12508=CARTESIAN_POINT('',(-6.,9.5,-0.4));
#12509=CARTESIAN_POINT('',(-6.,9.5,-0.4));
#12510=CARTESIAN_POINT('',(-6.,9.5,0.));
#12511=CARTESIAN_POINT('',(-6.,9.5,0.));
#12512=CARTESIAN_POINT('',(-6.,9.5,-0.4));
#12513=CARTESIAN_POINT('Origin',(-6.,10.5,-0.4));
#12514=CARTESIAN_POINT('',(-6.,10.5,-0.4));
#12515=CARTESIAN_POINT('',(-6.,10.5,0.));
#12516=CARTESIAN_POINT('Origin',(2.,10.,0.));
#12517=CARTESIAN_POINT('Origin',(2.,10.,-0.4));
#16945=UNCERTAINTY_MEASURE_WITH_UNIT(LENGTH_MEASURE(0.001),#17047,
'DISTANCE_ACCURACY_VALUE',
'Maximum model space distance between geometric entities at asserted c
onnectivities');
#16993=UNCERTAINTY_MEASURE_WITH_UNIT(LENGTH_MEASURE(0.001),#17047,
'DISTANCE_ACCURACY_VALUE',
'Maximum model space distance between geometric entities at asserted c
onnectivities');
#16998=(
GEOMETRIC_REPRESENTATION_CONTEXT(3)
GLOBAL_UNCERTAINTY_ASSIGNED_CONTEXT((#16945))
GLOBAL_UNIT_ASSIGNED_CONTEXT((#17047,#17049,#17050))
REPRESENTATION_CONTEXT('','3D')
);
#17046=(
GEOMETRIC_REPRESENTATION_CONTEXT(3)
GLOBAL_UNCERTAINTY_ASSIGNED_CONTEXT((#16993))
GLOBAL_UNIT_ASSIGNED_CONTEXT((#17047,#17049,#17050))
REPRESENTATION_CONTEXT('','3D')
);
#17047=(
LENGTH_UNIT()
NAMED_UNIT(*)
SI_UNIT(.CENTI.,.METRE.)
);
#17049=(
NAMED_UNIT(*)
PLANE_ANGLE_UNIT()
SI_UNIT($,.RADIAN.)
);
#17050=(
NAMED_UNIT(*)
SI_UNIT($,.STERADIAN.)
SOLID_ANGLE_UNIT()
);
#17055=SHAPE_DEFINITION_REPRESENTATION(#17107,#17262);
#17107=PRODUCT_DEFINITION_SHAPE('',$,#17315);
#17262=SHAPE_REPRESENTATION('',(#8788),#16998);
#17310=PRODUCT_DEFINITION_CONTEXT('part definition',#17468,'design');
#17315=PRODUCT_DEFINITION('Foot strip (1)','Foot strip (1)',#17367,#17310);
#17367=PRODUCT_DEFINITION_FORMATION('',$,#17474);
#17468=APPLICATION_CONTEXT(
'Core Data for Automotive Mechanical Design Process');
#17469=PRODUCT_CONTEXT('part definition',#17468,'mechanical');
#17474=PRODUCT('Foot strip (1)','Foot strip (1)','Foot strip (1)',(#17469));
#17571=COLOUR_RGB('Light Blue',0.38,0.62,0.78);
#17572=FILL_AREA_STYLE_COLOUR('',#17571);
#17573=FILL_AREA_STYLE('',(#17572));
#17574=SURFACE_STYLE_FILL_AREA(#17573);
#17575=SURFACE_SIDE_STYLE('',(#17574));
#17576=SURFACE_STYLE_USAGE(.BOTH.,#17575);
#17577=PRESENTATION_STYLE_ASSIGNMENT((#17576));
ENDSEC;
END-ISO-10303-21;
